ISO-10303-21;
HEADER;
/* Generated by software containing ST-Developer
 * from STEP Tools, Inc. (www.steptools.com) 
 */

FILE_DESCRIPTION(
/* description */ ('Pipe clamp stand with threaded column'),
/* implementation_level */ '2;1');

FILE_NAME(
/* name */ 'Flat Washer - M8.step',
/* time_stamp */ '2026-10-27T10:55:48-07:00',
/* author */ (''),
/* organization */ (''),
/* preprocessor_version */ 'ST-DEVELOPER v20.2',
/* originating_system */ 'Autodesk Translation Framework v15.17.0.0',
/* authorisation */ '');

FILE_SCHEMA (('AUTOMOTIVE_DESIGN { 1 0 10303 214 3 1 1 }'));
ENDSEC;

DATA;
#10=MECHANICAL_DESIGN_GEOMETRIC_PRESENTATION_REPRESENTATION('',(#765),#34433);
#713=SHAPE_REPRESENTATION_RELATIONSHIP('SRR','None',#34555,#735);
#735=ADVANCED_BREP_SHAPE_REPRESENTATION('',(#793),#34423);
#765=STYLED_ITEM('',(#34750),#793);
#793=MANIFOLD_SOLID_BREP('Body1',#8794);
#845=FACE_BOUND('',#1972,.T.);
#846=FACE_BOUND('',#1974,.T.);
#1002=PLANE('',#9568);
#1003=PLANE('',#9569);
#1436=FACE_OUTER_BOUND('',#1969,.T.);
#1437=FACE_OUTER_BOUND('',#1970,.T.);
#1438=FACE_OUTER_BOUND('',#1971,.T.);
#1439=FACE_OUTER_BOUND('',#1973,.T.);
#1969=EDGE_LOOP('',(#7505,#7506,#7507,#7508));
#1970=EDGE_LOOP('',(#7509,#7510,#7511,#7512));
#1971=EDGE_LOOP('',(#7513));
#1972=EDGE_LOOP('',(#7514));
#1973=EDGE_LOOP('',(#7515));
#1974=EDGE_LOOP('',(#7516));
#2578=LINE('',#28822,#3195);
#2579=LINE('',#28828,#3196);
#3195=VECTOR('',#11269,0.42);
#3196=VECTOR('',#11276,0.8);
#3420=CIRCLE('',#9563,0.42);
#3421=CIRCLE('',#9564,0.42);
#3422=CIRCLE('',#9566,0.8);
#3423=CIRCLE('',#9567,0.8);
#4106=VERTEX_POINT('',#28819);
#4107=VERTEX_POINT('',#28821);
#4108=VERTEX_POINT('',#28825);
#4109=VERTEX_POINT('',#28827);
#5266=EDGE_CURVE('',#4106,#4106,#3420,.T.);
#5267=EDGE_CURVE('',#4106,#4107,#2578,.T.);
#5268=EDGE_CURVE('',#4107,#4107,#3421,.T.);
#5269=EDGE_CURVE('',#4108,#4108,#3422,.T.);
#5270=EDGE_CURVE('',#4108,#4109,#2579,.T.);
#5271=EDGE_CURVE('',#4109,#4109,#3423,.T.);
#7505=ORIENTED_EDGE('',*,*,#5266,.F.);
#7506=ORIENTED_EDGE('',*,*,#5267,.T.);
#7507=ORIENTED_EDGE('',*,*,#5268,.T.);
#7508=ORIENTED_EDGE('',*,*,#5267,.F.);
#7509=ORIENTED_EDGE('',*,*,#5269,.F.);
#7510=ORIENTED_EDGE('',*,*,#5270,.T.);
#7511=ORIENTED_EDGE('',*,*,#5271,.T.);
#7512=ORIENTED_EDGE('',*,*,#5270,.F.);
#7513=ORIENTED_EDGE('',*,*,#5269,.T.);
#7514=ORIENTED_EDGE('',*,*,#5266,.T.);
#7515=ORIENTED_EDGE('',*,*,#5271,.F.);
#7516=ORIENTED_EDGE('',*,*,#5268,.F.);
#8238=CYLINDRICAL_SURFACE('',#9562,0.42);
#8239=CYLINDRICAL_SURFACE('',#9565,0.8);
#8673=ADVANCED_FACE('',(#1436),#8238,.F.);
#8674=ADVANCED_FACE('',(#1437),#8239,.T.);
#8675=ADVANCED_FACE('',(#1438,#845),#1002,.T.);
#8676=ADVANCED_FACE('',(#1439,#846),#1003,.F.);
#8794=CLOSED_SHELL('',(#8673,#8674,#8675,#8676));
#9561=AXIS2_PLACEMENT_3D('',#28817,#11263,#11264);
#9562=AXIS2_PLACEMENT_3D('',#28818,#11265,#11266);
#9563=AXIS2_PLACEMENT_3D('',#28820,#11267,#11268);
#9564=AXIS2_PLACEMENT_3D('',#28823,#11270,#11271);
#9565=AXIS2_PLACEMENT_3D('',#28824,#11272,#11273);
#9566=AXIS2_PLACEMENT_3D('',#28826,#11274,#11275);
#9567=AXIS2_PLACEMENT_3D('',#28829,#11277,#11278);
#9568=AXIS2_PLACEMENT_3D('',#28830,#11279,#11280);
#9569=AXIS2_PLACEMENT_3D('',#28831,#11281,#11282);
#11263=DIRECTION('axis',(0.,0.,1.));
#11264=DIRECTION('refdir',(1.,0.,0.));
#11265=DIRECTION('center_axis',(0.,1.,0.));
#11266=DIRECTION('ref_axis',(1.,0.,0.));
#11267=DIRECTION('center_axis',(0.,-1.,0.));
#11268=DIRECTION('ref_axis',(1.,0.,0.));
#11269=DIRECTION('',(0.,-1.,0.));
#11270=DIRECTION('center_axis',(0.,-1.,0.));
#11271=DIRECTION('ref_axis',(1.,0.,0.));
#11272=DIRECTION('center_axis',(0.,1.,0.));
#11273=DIRECTION('ref_axis',(1.,0.,0.));
#11274=DIRECTION('center_axis',(0.,1.,0.));
#11275=DIRECTION('ref_axis',(1.,0.,0.));
#11276=DIRECTION('',(0.,-1.,0.));
#11277=DIRECTION('center_axis',(0.,1.,0.));
#11278=DIRECTION('ref_axis',(1.,0.,0.));
#11279=DIRECTION('center_axis',(0.,1.,0.));
#11280=DIRECTION('ref_axis',(1.,0.,0.));
#11281=DIRECTION('center_axis',(0.,1.,0.));
#11282=DIRECTION('ref_axis',(1.,0.,0.));
#28817=CARTESIAN_POINT('',(0.,0.,0.));
#28818=CARTESIAN_POINT('Origin',(0.,0.,0.));
#28819=CARTESIAN_POINT('',(-0.42,0.16,5.14351655641888E-17));
#28820=CARTESIAN_POINT('Origin',(0.,0.16,0.));
#28821=CARTESIAN_POINT('',(-0.42,0.,5.14351655641888E-17));
#28822=CARTESIAN_POINT('',(-0.42,0.,5.14351655641888E-17));
#28823=CARTESIAN_POINT('Origin',(0.,0.,0.));
#28824=CARTESIAN_POINT('Origin',(0.,0.,0.));
#28825=CARTESIAN_POINT('',(-0.8,0.16,9.79717439317883E-17));
#28826=CARTESIAN_POINT('Origin',(0.,0.16,0.));
#28827=CARTESIAN_POINT('',(-0.8,0.,9.79717439317883E-17));
#28828=CARTESIAN_POINT('',(-0.8,0.,9.79717439317883E-17));
#28829=CARTESIAN_POINT('Origin',(0.,0.,0.));
#28830=CARTESIAN_POINT('Origin',(0.,0.16,0.));
#28831=CARTESIAN_POINT('Origin',(0.,0.,0.));
#34394=UNCERTAINTY_MEASURE_WITH_UNIT(LENGTH_MEASURE(0.001),#34434,
'DISTANCE_ACCURACY_VALUE',
'Maximum model space distance between geometric entities at asserted c
onnectivities');
#34404=UNCERTAINTY_MEASURE_WITH_UNIT(LENGTH_MEASURE(0.001),#34434,
'DISTANCE_ACCURACY_VALUE',
'Maximum model space distance between geometric entities at asserted c
onnectivities');
#34423=(
GEOMETRIC_REPRESENTATION_CONTEXT(3)
GLOBAL_UNCERTAINTY_ASSIGNED_CONTEXT((#34394))
GLOBAL_UNIT_ASSIGNED_CONTEXT((#34434,#34436,#34437))
REPRESENTATION_CONTEXT('','3D')
);
#34433=(
GEOMETRIC_REPRESENTATION_CONTEXT(3)
GLOBAL_UNCERTAINTY_ASSIGNED_CONTEXT((#34404))
GLOBAL_UNIT_ASSIGNED_CONTEXT((#34434,#34436,#34437))
REPRESENTATION_CONTEXT('','3D')
);
#34434=(
LENGTH_UNIT()
NAMED_UNIT(*)
SI_UNIT(.CENTI.,.METRE.)
);
#34436=(
NAMED_UNIT(*)
PLANE_ANGLE_UNIT()
SI_UNIT($,.RADIAN.)
);
#34437=(
NAMED_UNIT(*)
SI_UNIT($,.STERADIAN.)
SOLID_ANGLE_UNIT()
);
#34456=SHAPE_DEFINITION_REPRESENTATION(#34484,#34555);
#34484=PRODUCT_DEFINITION_SHAPE('',$,#34584);
#34555=SHAPE_REPRESENTATION('',(#9561),#34423);
#34565=PRODUCT_DEFINITION_CONTEXT('part definition',#34651,'design');
#34584=PRODUCT_DEFINITION('Flat Washer - M8','Flat Washer - M8',#34612,
#34565);
#34612=PRODUCT_DEFINITION_FORMATION('',$,#34671);
#34651=APPLICATION_CONTEXT(
'Core Data for Automotive Mechanical Design Process');
#34652=PRODUCT_CONTEXT('part definition',#34651,'mechanical');
#34671=PRODUCT('Flat Washer - M8','Flat Washer - M8','Flat Washer - M8',
(#34652));
#34744=COLOUR_RGB('Black',0.12,0.14,0.17);
#34745=FILL_AREA_STYLE_COLOUR('',#34744);
#34746=FILL_AREA_STYLE('',(#34745));
#34747=SURFACE_STYLE_FILL_AREA(#34746);
#34748=SURFACE_SIDE_STYLE('',(#34747));
#34749=SURFACE_STYLE_USAGE(.BOTH.,#34748);
#34750=PRESENTATION_STYLE_ASSIGNMENT((#34749));
ENDSEC;
END-ISO-10303-21;
